ISO-10303-21;
HEADER;
/* Generated by software containing ST-Developer
 * from STEP Tools, Inc. (www.steptools.com) 
 */

FILE_DESCRIPTION(
/* description */ ('STEP AP214'),
/* implementation_level */ '2;1');

FILE_NAME(
/* name */ 'PRT-TQ-1012-09.step',
/* time_stamp */ '2026-10-07T12:49:37-07:00',
/* author */ (''),
/* organization */ (''),
/* preprocessor_version */ 'ST-DEVELOPER v20.2',
/* originating_system */ 'Autodesk Translation Framework v15.15.0.0',
/* authorisation */ '');

FILE_SCHEMA (('AUTOMOTIVE_DESIGN { 1 0 10303 214 3 1 1 }'));
ENDSEC;

DATA;
#10=MECHANICAL_DESIGN_GEOMETRIC_PRESENTATION_REPRESENTATION('',(#307),#33016);
#249=SHAPE_REPRESENTATION_RELATIONSHIP('SRR','None',#33143,#276);
#276=ADVANCED_BREP_SHAPE_REPRESENTATION('',(#334),#33004);
#307=STYLED_ITEM('',(#33288),#334);
#334=MANIFOLD_SOLID_BREP('Body1',#9958);
#960=PLANE('',#10879);
#961=PLANE('',#10880);
#1393=FACE_OUTER_BOUND('',#1997,.T.);
#1394=FACE_OUTER_BOUND('',#1998,.T.);
#1395=FACE_OUTER_BOUND('',#1999,.T.);
#1997=EDGE_LOOP('',(#8300,#8301,#8302,#8303));
#1998=EDGE_LOOP('',(#8304));
#1999=EDGE_LOOP('',(#8305));
#2462=CIRCLE('',#10877,8.925);
#2463=CIRCLE('',#10878,8.925);
#3177=LINE('',#27965,#3927);
#3927=VECTOR('',#13032,8.925);
#4717=VERTEX_POINT('',#27962);
#4718=VERTEX_POINT('',#27964);
#5963=EDGE_CURVE('',#4717,#4717,#2462,.T.);
#5964=EDGE_CURVE('',#4717,#4718,#3177,.T.);
#5965=EDGE_CURVE('',#4718,#4718,#2463,.T.);
#8300=ORIENTED_EDGE('',*,*,#5963,.T.);
#8301=ORIENTED_EDGE('',*,*,#5964,.T.);
#8302=ORIENTED_EDGE('',*,*,#5965,.F.);
#8303=ORIENTED_EDGE('',*,*,#5964,.F.);
#8304=ORIENTED_EDGE('',*,*,#5965,.T.);
#8305=ORIENTED_EDGE('',*,*,#5963,.F.);
#9315=CYLINDRICAL_SURFACE('',#10876,8.925);
#9759=ADVANCED_FACE('',(#1393),#9315,.T.);
#9760=ADVANCED_FACE('',(#1394),#960,.T.);
#9761=ADVANCED_FACE('',(#1395),#961,.F.);
#9958=CLOSED_SHELL('',(#9759,#9760,#9761));
#10875=AXIS2_PLACEMENT_3D('',#27960,#13026,#13027);
#10876=AXIS2_PLACEMENT_3D('',#27961,#13028,#13029);
#10877=AXIS2_PLACEMENT_3D('',#27963,#13030,#13031);
#10878=AXIS2_PLACEMENT_3D('',#27966,#13033,#13034);
#10879=AXIS2_PLACEMENT_3D('',#27967,#13035,#13036);
#10880=AXIS2_PLACEMENT_3D('',#27968,#13037,#13038);
#13026=DIRECTION('axis',(0.,0.,1.));
#13027=DIRECTION('refdir',(1.,0.,0.));
#13028=DIRECTION('center_axis',(7.99859929422742E-44,-1.,0.));
#13029=DIRECTION('ref_axis',(-1.23541874016716E-29,-9.88161946317638E-73,
-1.));
#13030=DIRECTION('center_axis',(-7.99859929422742E-44,1.,0.));
#13031=DIRECTION('ref_axis',(1.23541874016716E-29,9.88161946317638E-73,
1.));
#13032=DIRECTION('',(-7.99859929422742E-44,1.,0.));
#13033=DIRECTION('center_axis',(-7.99859929422742E-44,1.,0.));
#13034=DIRECTION('ref_axis',(1.23541874016716E-29,9.88161946317638E-73,
1.));
#13035=DIRECTION('center_axis',(-7.99859929422742E-44,1.,9.88161946317638E-73));
#13036=DIRECTION('ref_axis',(1.23541874016716E-29,6.83612350571318E-90,
1.));
#13037=DIRECTION('center_axis',(-7.99859929422742E-44,1.,9.88161946317638E-73));
#13038=DIRECTION('ref_axis',(1.23541874016716E-29,6.83612350571318E-90,
1.));
#27960=CARTESIAN_POINT('',(0.,0.,0.));
#27961=CARTESIAN_POINT('Origin',(0.,1.90000000000001,-9.86076131526265E-29));
#27962=CARTESIAN_POINT('',(1.10261122559919E-28,0.,8.925));
#27963=CARTESIAN_POINT('Origin',(0.,0.,0.));
#27964=CARTESIAN_POINT('',(1.10261122559919E-28,1.90000000000001,8.925));
#27965=CARTESIAN_POINT('',(-1.0929972682389E-15,1.90000000000001,8.925));
#27966=CARTESIAN_POINT('Origin',(0.,1.90000000000001,-9.86076131526265E-29));
#27967=CARTESIAN_POINT('Origin',(0.,1.90000000000001,-9.86076131526265E-29));
#27968=CARTESIAN_POINT('Origin',(0.,0.,0.));
#32972=UNCERTAINTY_MEASURE_WITH_UNIT(LENGTH_MEASURE(0.01),#33017,
'DISTANCE_ACCURACY_VALUE',
'Maximum model space distance between geometric entities at asserted c
onnectivities');
#32984=UNCERTAINTY_MEASURE_WITH_UNIT(LENGTH_MEASURE(0.01),#33017,
'DISTANCE_ACCURACY_VALUE',
'Maximum model space distance between geometric entities at asserted c
onnectivities');
#33004=(
GEOMETRIC_REPRESENTATION_CONTEXT(3)
GLOBAL_UNCERTAINTY_ASSIGNED_CONTEXT((#32972))
GLOBAL_UNIT_ASSIGNED_CONTEXT((#33017,#33019,#33020))
REPRESENTATION_CONTEXT('','3D')
);
#33016=(
GEOMETRIC_REPRESENTATION_CONTEXT(3)
GLOBAL_UNCERTAINTY_ASSIGNED_CONTEXT((#32984))
GLOBAL_UNIT_ASSIGNED_CONTEXT((#33017,#33019,#33020))
REPRESENTATION_CONTEXT('','3D')
);
#33017=(
LENGTH_UNIT()
NAMED_UNIT(*)
SI_UNIT(.MILLI.,.METRE.)
);
#33019=(
NAMED_UNIT(*)
PLANE_ANGLE_UNIT()
SI_UNIT($,.RADIAN.)
);
#33020=(
NAMED_UNIT(*)
SI_UNIT($,.STERADIAN.)
SOLID_ANGLE_UNIT()
);
#33040=SHAPE_DEFINITION_REPRESENTATION(#33079,#33143);
#33079=PRODUCT_DEFINITION_SHAPE('',$,#33175);
#33143=SHAPE_REPRESENTATION('',(#10875),#33004);
#33155=PRODUCT_DEFINITION_CONTEXT('part definition',#33250,'design');
#33175=PRODUCT_DEFINITION(
'P_Torque Wrench_Push Plate_PRT-TQ-1012-09_M_Rev00','PRT-TQ-1012-09',#33206,
#33155);
#33206=PRODUCT_DEFINITION_FORMATION('',$,#33271);
#33250=APPLICATION_CONTEXT(
'Core Data for Automotive Mechanical Design Process');
#33251=PRODUCT_CONTEXT('part definition',#33250,'mechanical');
#33271=PRODUCT('P_Torque Wrench_Push Plate_PRT-TQ-1012-09_M_Rev00',
'PRT-TQ-1012-09',$,(#33251));
#33288=PRESENTATION_STYLE_ASSIGNMENT((#33295));
#33295=SURFACE_STYLE_USAGE(.BOTH.,#33302);
#33302=SURFACE_SIDE_STYLE('',(#33309));
#33309=SURFACE_STYLE_FILL_AREA(#33316);
#33316=FILL_AREA_STYLE('Opaque(192,192,192)',(#33323));
#33323=FILL_AREA_STYLE_COLOUR('Opaque(192,192,192)',#33330);
#33330=COLOUR_RGB('Opaque(192,192,192)', 0.72549020, 0.75294118, 0.79215686);
ENDSEC;
END-ISO-10303-21;
